ISO-10303-21;
HEADER;
/* Generated by software containing ST-Developer
 * from STEP Tools, Inc. (www.steptools.com) 
 */

FILE_DESCRIPTION(
/* description */ ('Torque wrench calibration arm'),
/* implementation_level */ '2;1');

FILE_NAME(
/* name */ 'Cap Screw - M4x16.step',
/* time_stamp */ '2026-10-28T03:24:52-07:00',
/* author */ (''),
/* organization */ (''),
/* preprocessor_version */ 'ST-DEVELOPER v20.2',
/* originating_system */ 'Autodesk Translation Framework v15.17.0.0',
/* authorisation */ '');

FILE_SCHEMA (('AUTOMOTIVE_DESIGN { 1 0 10303 214 3 1 1 }'));
ENDSEC;

DATA;
#10=MECHANICAL_DESIGN_GEOMETRIC_PRESENTATION_REPRESENTATION('',(#448),#12783);
#12=ORIENTED_CLOSED_SHELL('',*,#6519,.F.);
#15=BREP_WITH_VOIDS('Body1',#6518,(#12));
#335=CONICAL_SURFACE('',#7330,0.325,0.785398163397448);
#336=CONICAL_SURFACE('',#7334,0.335,0.785398163397448);
#337=CONICAL_SURFACE('',#7338,0.21,0.463647609000806);
#338=CONICAL_SURFACE('',#7342,0.18,0.785398163397448);
#365=SHAPE_REPRESENTATION_RELATIONSHIP('SRR','None',#12947,#402);
#402=ADVANCED_BREP_SHAPE_REPRESENTATION('',(#15),#12756);
#448=STYLED_ITEM('',(#13219),#15);
#593=FACE_BOUND('',#1508,.T.);
#739=PLANE('',#7328);
#740=PLANE('',#7336);
#741=PLANE('',#7344);
#742=PLANE('',#7345);
#743=PLANE('',#7346);
#744=PLANE('',#7347);
#745=PLANE('',#7348);
#746=PLANE('',#7349);
#747=PLANE('',#7350);
#748=PLANE('',#7351);
#749=PLANE('',#7352);
#1046=FACE_OUTER_BOUND('',#1503,.T.);
#1047=FACE_OUTER_BOUND('',#1504,.T.);
#1048=FACE_OUTER_BOUND('',#1505,.T.);
#1049=FACE_OUTER_BOUND('',#1506,.T.);
#1050=FACE_OUTER_BOUND('',#1507,.T.);
#1051=FACE_OUTER_BOUND('',#1509,.T.);
#1052=FACE_OUTER_BOUND('',#1510,.T.);
#1053=FACE_OUTER_BOUND('',#1511,.T.);
#1054=FACE_OUTER_BOUND('',#1512,.T.);
#1055=FACE_OUTER_BOUND('',#1513,.T.);
#1056=FACE_OUTER_BOUND('',#1514,.T.);
#1057=FACE_OUTER_BOUND('',#1515,.T.);
#1058=FACE_OUTER_BOUND('',#1516,.T.);
#1059=FACE_OUTER_BOUND('',#1517,.T.);
#1060=FACE_OUTER_BOUND('',#1518,.T.);
#1061=FACE_OUTER_BOUND('',#1519,.T.);
#1062=FACE_OUTER_BOUND('',#1520,.T.);
#1503=EDGE_LOOP('',(#5085));
#1504=EDGE_LOOP('',(#5086,#5087,#5088,#5089));
#1505=EDGE_LOOP('',(#5090,#5091,#5092,#5093));
#1506=EDGE_LOOP('',(#5094,#5095,#5096,#5097));
#1507=EDGE_LOOP('',(#5098));
#1508=EDGE_LOOP('',(#5099));
#1509=EDGE_LOOP('',(#5100,#5101,#5102,#5103));
#1510=EDGE_LOOP('',(#5104,#5105,#5106,#5107));
#1511=EDGE_LOOP('',(#5108,#5109,#5110,#5111));
#1512=EDGE_LOOP('',(#5112));
#1513=EDGE_LOOP('',(#5113,#5114,#5115,#5116));
#1514=EDGE_LOOP('',(#5117,#5118,#5119,#5120));
#1515=EDGE_LOOP('',(#5121,#5122,#5123,#5124));
#1516=EDGE_LOOP('',(#5125,#5126,#5127,#5128));
#1517=EDGE_LOOP('',(#5129,#5130,#5131,#5132));
#1518=EDGE_LOOP('',(#5133,#5134,#5135,#5136));
#1519=EDGE_LOOP('',(#5137,#5138,#5139,#5140,#5141,#5142));
#1520=EDGE_LOOP('',(#5143,#5144,#5145,#5146,#5147,#5148));
#1960=LINE('',#11123,#2375);
#1961=LINE('',#11127,#2376);
#1962=LINE('',#11131,#2377);
#1963=LINE('',#11138,#2378);
#1964=LINE('',#11142,#2379);
#1965=LINE('',#11146,#2380);
#1966=LINE('',#11151,#2381);
#1967=LINE('',#11153,#2382);
#1968=LINE('',#11155,#2383);
#1969=LINE('',#11156,#2384);
#1970=LINE('',#11159,#2385);
#1971=LINE('',#11161,#2386);
#1972=LINE('',#11162,#2387);
#1973=LINE('',#11165,#2388);
#1974=LINE('',#11167,#2389);
#1975=LINE('',#11168,#2390);
#1976=LINE('',#11171,#2391);
#1977=LINE('',#11173,#2392);
#1978=LINE('',#11174,#2393);
#1979=LINE('',#11177,#2394);
#1980=LINE('',#11179,#2395);
#1981=LINE('',#11180,#2396);
#1982=LINE('',#11182,#2397);
#1983=LINE('',#11183,#2398);
#2375=VECTOR('',#8728,0.325);
#2376=VECTOR('',#8733,0.35);
#2377=VECTOR('',#8738,0.335);
#2378=VECTOR('',#8747,0.21);
#2379=VECTOR('',#8752,0.2);
#2380=VECTOR('',#8757,0.18);
#2381=VECTOR('',#8762,1.);
#2382=VECTOR('',#8763,1.);
#2383=VECTOR('',#8764,1.);
#2384=VECTOR('',#8765,1.);
#2385=VECTOR('',#8768,1.);
#2386=VECTOR('',#8769,1.);
#2387=VECTOR('',#8770,1.);
#2388=VECTOR('',#8773,1.);
#2389=VECTOR('',#8774,1.);
#2390=VECTOR('',#8775,1.);
#2391=VECTOR('',#8778,1.);
#2392=VECTOR('',#8779,1.);
#2393=VECTOR('',#8780,1.);
#2394=VECTOR('',#8783,1.);
#2395=VECTOR('',#8784,1.);
#2396=VECTOR('',#8785,1.);
#2397=VECTOR('',#8788,1.);
#2398=VECTOR('',#8789,1.);
#2791=CIRCLE('',#7329,0.3);
#2792=CIRCLE('',#7331,0.35);
#2793=CIRCLE('',#7333,0.35);
#2794=CIRCLE('',#7335,0.32);
#2795=CIRCLE('',#7337,0.22);
#2796=CIRCLE('',#7339,0.1954);
#2797=CIRCLE('',#7341,0.1954);
#2798=CIRCLE('',#7343,0.16);
#3225=VERTEX_POINT('',#11118);
#3226=VERTEX_POINT('',#11121);
#3227=VERTEX_POINT('',#11125);
#3228=VERTEX_POINT('',#11129);
#3229=VERTEX_POINT('',#11133);
#3230=VERTEX_POINT('',#11136);
#3231=VERTEX_POINT('',#11140);
#3232=VERTEX_POINT('',#11144);
#3233=VERTEX_POINT('',#11149);
#3234=VERTEX_POINT('',#11150);
#3235=VERTEX_POINT('',#11152);
#3236=VERTEX_POINT('',#11154);
#3237=VERTEX_POINT('',#11158);
#3238=VERTEX_POINT('',#11160);
#3239=VERTEX_POINT('',#11164);
#3240=VERTEX_POINT('',#11166);
#3241=VERTEX_POINT('',#11170);
#3242=VERTEX_POINT('',#11172);
#3243=VERTEX_POINT('',#11176);
#3244=VERTEX_POINT('',#11178);
#3900=EDGE_CURVE('',#3225,#3225,#2791,.T.);
#3901=EDGE_CURVE('',#3226,#3226,#2792,.T.);
#3902=EDGE_CURVE('',#3226,#3225,#1960,.T.);
#3903=EDGE_CURVE('',#3227,#3227,#2793,.T.);
#3904=EDGE_CURVE('',#3227,#3226,#1961,.T.);
#3905=EDGE_CURVE('',#3228,#3228,#2794,.T.);
#3906=EDGE_CURVE('',#3228,#3227,#1962,.T.);
#3907=EDGE_CURVE('',#3229,#3229,#2795,.T.);
#3908=EDGE_CURVE('',#3230,#3230,#2796,.F.);
#3909=EDGE_CURVE('',#3230,#3229,#1963,.T.);
#3910=EDGE_CURVE('',#3231,#3231,#2797,.F.);
#3911=EDGE_CURVE('',#3231,#3230,#1964,.T.);
#3912=EDGE_CURVE('',#3232,#3232,#2798,.T.);
#3913=EDGE_CURVE('',#3232,#3231,#1965,.T.);
#3914=EDGE_CURVE('',#3233,#3234,#1966,.T.);
#3915=EDGE_CURVE('',#3234,#3235,#1967,.T.);
#3916=EDGE_CURVE('',#3235,#3236,#1968,.T.);
#3917=EDGE_CURVE('',#3233,#3236,#1969,.T.);
#3918=EDGE_CURVE('',#3234,#3237,#1970,.T.);
#3919=EDGE_CURVE('',#3237,#3238,#1971,.T.);
#3920=EDGE_CURVE('',#3238,#3235,#1972,.T.);
#3921=EDGE_CURVE('',#3237,#3239,#1973,.T.);
#3922=EDGE_CURVE('',#3239,#3240,#1974,.T.);
#3923=EDGE_CURVE('',#3240,#3238,#1975,.T.);
#3924=EDGE_CURVE('',#3239,#3241,#1976,.T.);
#3925=EDGE_CURVE('',#3241,#3242,#1977,.T.);
#3926=EDGE_CURVE('',#3242,#3240,#1978,.T.);
#3927=EDGE_CURVE('',#3241,#3243,#1979,.T.);
#3928=EDGE_CURVE('',#3243,#3244,#1980,.T.);
#3929=EDGE_CURVE('',#3244,#3242,#1981,.T.);
#3930=EDGE_CURVE('',#3243,#3233,#1982,.T.);
#3931=EDGE_CURVE('',#3236,#3244,#1983,.T.);
#5085=ORIENTED_EDGE('',*,*,#3900,.F.);
#5086=ORIENTED_EDGE('',*,*,#3901,.F.);
#5087=ORIENTED_EDGE('',*,*,#3902,.T.);
#5088=ORIENTED_EDGE('',*,*,#3900,.T.);
#5089=ORIENTED_EDGE('',*,*,#3902,.F.);
#5090=ORIENTED_EDGE('',*,*,#3903,.F.);
#5091=ORIENTED_EDGE('',*,*,#3904,.T.);
#5092=ORIENTED_EDGE('',*,*,#3901,.T.);
#5093=ORIENTED_EDGE('',*,*,#3904,.F.);
#5094=ORIENTED_EDGE('',*,*,#3905,.F.);
#5095=ORIENTED_EDGE('',*,*,#3906,.T.);
#5096=ORIENTED_EDGE('',*,*,#3903,.T.);
#5097=ORIENTED_EDGE('',*,*,#3906,.F.);
#5098=ORIENTED_EDGE('',*,*,#3905,.T.);
#5099=ORIENTED_EDGE('',*,*,#3907,.F.);
#5100=ORIENTED_EDGE('',*,*,#3908,.F.);
#5101=ORIENTED_EDGE('',*,*,#3909,.T.);
#5102=ORIENTED_EDGE('',*,*,#3907,.T.);
#5103=ORIENTED_EDGE('',*,*,#3909,.F.);
#5104=ORIENTED_EDGE('',*,*,#3910,.F.);
#5105=ORIENTED_EDGE('',*,*,#3911,.T.);
#5106=ORIENTED_EDGE('',*,*,#3908,.T.);
#5107=ORIENTED_EDGE('',*,*,#3911,.F.);
#5108=ORIENTED_EDGE('',*,*,#3912,.F.);
#5109=ORIENTED_EDGE('',*,*,#3913,.T.);
#5110=ORIENTED_EDGE('',*,*,#3910,.T.);
#5111=ORIENTED_EDGE('',*,*,#3913,.F.);
#5112=ORIENTED_EDGE('',*,*,#3912,.T.);
#5113=ORIENTED_EDGE('',*,*,#3914,.T.);
#5114=ORIENTED_EDGE('',*,*,#3915,.T.);
#5115=ORIENTED_EDGE('',*,*,#3916,.T.);
#5116=ORIENTED_EDGE('',*,*,#3917,.F.);
#5117=ORIENTED_EDGE('',*,*,#3918,.T.);
#5118=ORIENTED_EDGE('',*,*,#3919,.T.);
#5119=ORIENTED_EDGE('',*,*,#3920,.T.);
#5120=ORIENTED_EDGE('',*,*,#3915,.F.);
#5121=ORIENTED_EDGE('',*,*,#3921,.T.);
#5122=ORIENTED_EDGE('',*,*,#3922,.T.);
#5123=ORIENTED_EDGE('',*,*,#3923,.T.);
#5124=ORIENTED_EDGE('',*,*,#3919,.F.);
#5125=ORIENTED_EDGE('',*,*,#3924,.T.);
#5126=ORIENTED_EDGE('',*,*,#3925,.T.);
#5127=ORIENTED_EDGE('',*,*,#3926,.T.);
#5128=ORIENTED_EDGE('',*,*,#3922,.F.);
#5129=ORIENTED_EDGE('',*,*,#3927,.T.);
#5130=ORIENTED_EDGE('',*,*,#3928,.T.);
#5131=ORIENTED_EDGE('',*,*,#3929,.T.);
#5132=ORIENTED_EDGE('',*,*,#3925,.F.);
#5133=ORIENTED_EDGE('',*,*,#3930,.T.);
#5134=ORIENTED_EDGE('',*,*,#3917,.T.);
#5135=ORIENTED_EDGE('',*,*,#3931,.T.);
#5136=ORIENTED_EDGE('',*,*,#3928,.F.);
#5137=ORIENTED_EDGE('',*,*,#3930,.F.);
#5138=ORIENTED_EDGE('',*,*,#3927,.F.);
#5139=ORIENTED_EDGE('',*,*,#3924,.F.);
#5140=ORIENTED_EDGE('',*,*,#3921,.F.);
#5141=ORIENTED_EDGE('',*,*,#3918,.F.);
#5142=ORIENTED_EDGE('',*,*,#3914,.F.);
#5143=ORIENTED_EDGE('',*,*,#3931,.F.);
#5144=ORIENTED_EDGE('',*,*,#3916,.F.);
#5145=ORIENTED_EDGE('',*,*,#3920,.F.);
#5146=ORIENTED_EDGE('',*,*,#3923,.F.);
#5147=ORIENTED_EDGE('',*,*,#3926,.F.);
#5148=ORIENTED_EDGE('',*,*,#3929,.F.);
#6043=CYLINDRICAL_SURFACE('',#7332,0.35);
#6044=CYLINDRICAL_SURFACE('',#7340,0.1954);
#6271=ADVANCED_FACE('',(#1046),#739,.T.);
#6272=ADVANCED_FACE('',(#1047),#335,.T.);
#6273=ADVANCED_FACE('',(#1048),#6043,.T.);
#6274=ADVANCED_FACE('',(#1049),#336,.T.);
#6275=ADVANCED_FACE('',(#1050,#593),#740,.T.);
#6276=ADVANCED_FACE('',(#1051),#337,.T.);
#6277=ADVANCED_FACE('',(#1052),#6044,.T.);
#6278=ADVANCED_FACE('',(#1053),#338,.T.);
#6279=ADVANCED_FACE('',(#1054),#741,.T.);
#6280=ADVANCED_FACE('',(#1055),#742,.F.);
#6281=ADVANCED_FACE('',(#1056),#743,.F.);
#6282=ADVANCED_FACE('',(#1057),#744,.F.);
#6283=ADVANCED_FACE('',(#1058),#745,.F.);
#6284=ADVANCED_FACE('',(#1059),#746,.F.);
#6285=ADVANCED_FACE('',(#1060),#747,.F.);
#6286=ADVANCED_FACE('',(#1061),#748,.F.);
#6287=ADVANCED_FACE('',(#1062),#749,.F.);
#6518=CLOSED_SHELL('',(#6271,#6272,#6273,#6274,#6275,#6276,#6277,#6278,
#6279));
#6519=CLOSED_SHELL('',(#6280,#6281,#6282,#6283,#6284,#6285,#6286,#6287));
#7327=AXIS2_PLACEMENT_3D('',#11116,#8718,#8719);
#7328=AXIS2_PLACEMENT_3D('',#11117,#8720,#8721);
#7329=AXIS2_PLACEMENT_3D('',#11119,#8722,#8723);
#7330=AXIS2_PLACEMENT_3D('',#11120,#8724,#8725);
#7331=AXIS2_PLACEMENT_3D('',#11122,#8726,#8727);
#7332=AXIS2_PLACEMENT_3D('',#11124,#8729,#8730);
#7333=AXIS2_PLACEMENT_3D('',#11126,#8731,#8732);
#7334=AXIS2_PLACEMENT_3D('',#11128,#8734,#8735);
#7335=AXIS2_PLACEMENT_3D('',#11130,#8736,#8737);
#7336=AXIS2_PLACEMENT_3D('',#11132,#8739,#8740);
#7337=AXIS2_PLACEMENT_3D('',#11134,#8741,#8742);
#7338=AXIS2_PLACEMENT_3D('',#11135,#8743,#8744);
#7339=AXIS2_PLACEMENT_3D('',#11137,#8745,#8746);
#7340=AXIS2_PLACEMENT_3D('',#11139,#8748,#8749);
#7341=AXIS2_PLACEMENT_3D('',#11141,#8750,#8751);
#7342=AXIS2_PLACEMENT_3D('',#11143,#8753,#8754);
#7343=AXIS2_PLACEMENT_3D('',#11145,#8755,#8756);
#7344=AXIS2_PLACEMENT_3D('',#11147,#8758,#8759);
#7345=AXIS2_PLACEMENT_3D('',#11148,#8760,#8761);
#7346=AXIS2_PLACEMENT_3D('',#11157,#8766,#8767);
#7347=AXIS2_PLACEMENT_3D('',#11163,#8771,#8772);
#7348=AXIS2_PLACEMENT_3D('',#11169,#8776,#8777);
#7349=AXIS2_PLACEMENT_3D('',#11175,#8781,#8782);
#7350=AXIS2_PLACEMENT_3D('',#11181,#8786,#8787);
#7351=AXIS2_PLACEMENT_3D('',#11184,#8790,#8791);
#7352=AXIS2_PLACEMENT_3D('',#11185,#8792,#8793);
#8718=DIRECTION('axis',(0.,0.,1.));
#8719=DIRECTION('refdir',(1.,0.,0.));
#8720=DIRECTION('center_axis',(0.,1.,0.));
#8721=DIRECTION('ref_axis',(0.,0.,1.));
#8722=DIRECTION('center_axis',(0.,-1.,0.));
#8723=DIRECTION('ref_axis',(1.,0.,0.));
#8724=DIRECTION('center_axis',(0.,-1.,0.));
#8725=DIRECTION('ref_axis',(1.,0.,0.));
#8726=DIRECTION('center_axis',(0.,-1.,0.));
#8727=DIRECTION('ref_axis',(1.,0.,0.));
#8728=DIRECTION('',(0.707106781186547,0.707106781186548,8.65956056235493E-17));
#8729=DIRECTION('center_axis',(0.,-1.,0.));
#8730=DIRECTION('ref_axis',(1.,0.,0.));
#8731=DIRECTION('center_axis',(0.,-1.,0.));
#8732=DIRECTION('ref_axis',(1.,0.,0.));
#8733=DIRECTION('',(0.,1.,0.));
#8734=DIRECTION('center_axis',(0.,1.,0.));
#8735=DIRECTION('ref_axis',(1.,0.,0.));
#8736=DIRECTION('center_axis',(0.,-1.,0.));
#8737=DIRECTION('ref_axis',(1.,0.,0.));
#8738=DIRECTION('',(-0.707106781186547,0.707106781186548,-8.65956056235493E-17));
#8739=DIRECTION('center_axis',(0.,-1.,0.));
#8740=DIRECTION('ref_axis',(0.,0.,-1.));
#8741=DIRECTION('center_axis',(0.,-1.,0.));
#8742=DIRECTION('ref_axis',(1.,0.,0.));
#8743=DIRECTION('center_axis',(0.,1.,0.));
#8744=DIRECTION('ref_axis',(1.,0.,0.));
#8745=DIRECTION('center_axis',(0.,1.,0.));
#8746=DIRECTION('ref_axis',(1.,0.,0.));
#8747=DIRECTION('',(-0.447213595499958,0.894427190999916,-5.47678698264203E-17));
#8748=DIRECTION('center_axis',(0.,-1.,0.));
#8749=DIRECTION('ref_axis',(1.,0.,0.));
#8750=DIRECTION('center_axis',(0.,1.,0.));
#8751=DIRECTION('ref_axis',(1.,0.,0.));
#8752=DIRECTION('',(0.,1.,0.));
#8753=DIRECTION('center_axis',(0.,1.,0.));
#8754=DIRECTION('ref_axis',(1.,0.,0.));
#8755=DIRECTION('center_axis',(0.,-1.,0.));
#8756=DIRECTION('ref_axis',(1.,0.,0.));
#8757=DIRECTION('',(-0.707106781186547,0.707106781186548,-8.65956056235493E-17));
#8758=DIRECTION('center_axis',(0.,-1.,0.));
#8759=DIRECTION('ref_axis',(0.,0.,-1.));
#8760=DIRECTION('center_axis',(0.866025403784439,0.,-0.5));
#8761=DIRECTION('ref_axis',(0.5,0.,0.866025403784439));
#8762=DIRECTION('',(-0.5,0.,-0.866025403784439));
#8763=DIRECTION('',(0.,-1.,0.));
#8764=DIRECTION('',(0.5,0.,0.866025403784439));
#8765=DIRECTION('',(0.,-1.,0.));
#8766=DIRECTION('center_axis',(1.60246890531964E-16,0.,-1.));
#8767=DIRECTION('ref_axis',(1.,0.,1.60246890531964E-16));
#8768=DIRECTION('',(-1.,0.,-1.60246890531964E-16));
#8769=DIRECTION('',(0.,-1.,0.));
#8770=DIRECTION('',(1.,0.,1.60246890531964E-16));
#8771=DIRECTION('center_axis',(-0.866025403784439,0.,-0.5));
#8772=DIRECTION('ref_axis',(0.5,0.,-0.866025403784439));
#8773=DIRECTION('',(-0.5,0.,0.866025403784439));
#8774=DIRECTION('',(0.,-1.,0.));
#8775=DIRECTION('',(0.5,0.,-0.866025403784439));
#8776=DIRECTION('center_axis',(-0.866025403784439,0.,0.5));
#8777=DIRECTION('ref_axis',(-0.5,0.,-0.866025403784439));
#8778=DIRECTION('',(0.5,0.,0.866025403784439));
#8779=DIRECTION('',(0.,-1.,0.));
#8780=DIRECTION('',(-0.5,0.,-0.866025403784439));
#8781=DIRECTION('center_axis',(-1.60246890531964E-16,0.,1.));
#8782=DIRECTION('ref_axis',(-1.,0.,-1.60246890531964E-16));
#8783=DIRECTION('',(1.,0.,1.60246890531964E-16));
#8784=DIRECTION('',(0.,-1.,0.));
#8785=DIRECTION('',(-1.,0.,-1.60246890531964E-16));
#8786=DIRECTION('center_axis',(0.866025403784439,0.,0.5));
#8787=DIRECTION('ref_axis',(-0.5,0.,0.866025403784439));
#8788=DIRECTION('',(0.5,0.,-0.866025403784439));
#8789=DIRECTION('',(-0.5,0.,0.866025403784439));
#8790=DIRECTION('center_axis',(0.,1.,0.));
#8791=DIRECTION('ref_axis',(1.,0.,0.));
#8792=DIRECTION('center_axis',(0.,-1.,0.));
#8793=DIRECTION('ref_axis',(0.,0.,-1.));
#11116=CARTESIAN_POINT('',(0.,0.,0.));
#11117=CARTESIAN_POINT('Origin',(0.3,0.4,0.));
#11118=CARTESIAN_POINT('',(-0.3,0.4,-3.67394039744206E-17));
#11119=CARTESIAN_POINT('Origin',(0.,0.4,0.));
#11120=CARTESIAN_POINT('Origin',(0.,0.375,0.));
#11121=CARTESIAN_POINT('',(-0.35,0.35,-4.28626379701573E-17));
#11122=CARTESIAN_POINT('Origin',(0.,0.35,0.));
#11123=CARTESIAN_POINT('',(-0.325,0.375,-3.9801020972289E-17));
#11124=CARTESIAN_POINT('Origin',(0.,0.19,0.));
#11125=CARTESIAN_POINT('',(-0.35,0.03,-4.28626379701574E-17));
#11126=CARTESIAN_POINT('Origin',(0.,0.03,0.));
#11127=CARTESIAN_POINT('',(-0.35,0.19,-4.28626379701574E-17));
#11128=CARTESIAN_POINT('Origin',(0.,0.0149999999999999,0.));
#11129=CARTESIAN_POINT('',(-0.32,-3.29597460435593E-17,-3.91886975727153E-17));
#11130=CARTESIAN_POINT('Origin',(0.,0.,0.));
#11131=CARTESIAN_POINT('',(-0.335,0.0149999999999999,-4.10256677714363E-17));
#11132=CARTESIAN_POINT('Origin',(0.22,0.,0.));
#11133=CARTESIAN_POINT('',(-0.22,-6.93889390390723E-18,-2.69422295812418E-17));
#11134=CARTESIAN_POINT('Origin',(0.,0.,0.));
#11135=CARTESIAN_POINT('Origin',(0.,-0.02,0.));
#11136=CARTESIAN_POINT('',(-0.1954,-0.0492,2.39295984553393E-17));
#11137=CARTESIAN_POINT('Origin',(0.,-0.0492,0.));
#11138=CARTESIAN_POINT('',(-0.21,-0.02,-2.57175827820944E-17));
#11139=CARTESIAN_POINT('Origin',(0.,-0.8,0.));
#11140=CARTESIAN_POINT('',(-0.1954,-1.5646,2.39295984553393E-17));
#11141=CARTESIAN_POINT('Origin',(0.,-1.5646,0.));
#11142=CARTESIAN_POINT('',(-0.1954,-0.8,-2.39295984553393E-17));
#11143=CARTESIAN_POINT('Origin',(0.,-1.58,0.));
#11144=CARTESIAN_POINT('',(-0.16,-1.6,-1.95943487863577E-17));
#11145=CARTESIAN_POINT('Origin',(0.,-1.6,0.));
#11146=CARTESIAN_POINT('',(-0.18,-1.58,-2.20436423846524E-17));
#11147=CARTESIAN_POINT('Origin',(0.,-1.6,0.));
#11148=CARTESIAN_POINT('Origin',(0.0866025403784439,-0.4,-0.15));
#11149=CARTESIAN_POINT('',(0.173205080756888,-0.4,0.));
#11150=CARTESIAN_POINT('',(0.0866025403784439,-0.4,-0.15));
#11151=CARTESIAN_POINT('',(0.173205080756888,-0.4,0.));
#11152=CARTESIAN_POINT('',(0.0866025403784439,-0.64,-0.15));
#11153=CARTESIAN_POINT('',(0.0866025403784439,-0.4,-0.15));
#11154=CARTESIAN_POINT('',(0.173205080756888,-0.64,0.));
#11155=CARTESIAN_POINT('',(0.173205080756888,-0.64,0.));
#11156=CARTESIAN_POINT('',(0.173205080756888,-0.4,0.));
#11157=CARTESIAN_POINT('Origin',(-0.0866025403784438,-0.4,-0.15));
#11158=CARTESIAN_POINT('',(-0.0866025403784438,-0.4,-0.15));
#11159=CARTESIAN_POINT('',(0.0866025403784439,-0.4,-0.15));
#11160=CARTESIAN_POINT('',(-0.0866025403784438,-0.64,-0.15));
#11161=CARTESIAN_POINT('',(-0.0866025403784438,-0.4,-0.15));
#11162=CARTESIAN_POINT('',(0.0866025403784439,-0.64,-0.15));
#11163=CARTESIAN_POINT('Origin',(-0.173205080756888,-0.4,-2.77555756156289E-17));
#11164=CARTESIAN_POINT('',(-0.173205080756888,-0.4,-2.12115047744981E-17));
#11165=CARTESIAN_POINT('',(-0.0866025403784438,-0.4,-0.15));
#11166=CARTESIAN_POINT('',(-0.173205080756888,-0.64,-2.77555756156289E-17));
#11167=CARTESIAN_POINT('',(-0.173205080756888,-0.4,-2.12115047744981E-17));
#11168=CARTESIAN_POINT('',(-0.0866025403784438,-0.64,-0.15));
#11169=CARTESIAN_POINT('Origin',(-0.0866025403784439,-0.4,0.15));
#11170=CARTESIAN_POINT('',(-0.0866025403784439,-0.4,0.15));
#11171=CARTESIAN_POINT('',(-0.173205080756888,-0.4,-2.12115047744981E-17));
#11172=CARTESIAN_POINT('',(-0.0866025403784439,-0.64,0.15));
#11173=CARTESIAN_POINT('',(-0.0866025403784439,-0.4,0.15));
#11174=CARTESIAN_POINT('',(-0.173205080756888,-0.64,-2.12115047744981E-17));
#11175=CARTESIAN_POINT('Origin',(0.0866025403784439,-0.4,0.15));
#11176=CARTESIAN_POINT('',(0.0866025403784439,-0.4,0.15));
#11177=CARTESIAN_POINT('',(-0.0866025403784439,-0.4,0.15));
#11178=CARTESIAN_POINT('',(0.0866025403784439,-0.64,0.15));
#11179=CARTESIAN_POINT('',(0.0866025403784439,-0.4,0.15));
#11180=CARTESIAN_POINT('',(-0.0866025403784439,-0.64,0.15));
#11181=CARTESIAN_POINT('Origin',(0.173205080756888,-0.4,0.));
#11182=CARTESIAN_POINT('',(0.0866025403784439,-0.4,0.15));
#11183=CARTESIAN_POINT('',(0.0866025403784439,-0.64,0.15));
#11184=CARTESIAN_POINT('Origin',(0.,-0.4,-2.77555756156289E-17));
#11185=CARTESIAN_POINT('Origin',(0.,-0.64,-2.77555756156289E-17));
#12712=UNCERTAINTY_MEASURE_WITH_UNIT(LENGTH_MEASURE(0.001),#12784,
'DISTANCE_ACCURACY_VALUE',
'Maximum model space distance between geometric entities at asserted c
onnectivities');
#12739=UNCERTAINTY_MEASURE_WITH_UNIT(LENGTH_MEASURE(0.001),#12784,
'DISTANCE_ACCURACY_VALUE',
'Maximum model space distance between geometric entities at asserted c
onnectivities');
#12756=(
GEOMETRIC_REPRESENTATION_CONTEXT(3)
GLOBAL_UNCERTAINTY_ASSIGNED_CONTEXT((#12712))
GLOBAL_UNIT_ASSIGNED_CONTEXT((#12784,#12786,#12787))
REPRESENTATION_CONTEXT('','3D')
);
#12783=(
GEOMETRIC_REPRESENTATION_CONTEXT(3)
GLOBAL_UNCERTAINTY_ASSIGNED_CONTEXT((#12739))
GLOBAL_UNIT_ASSIGNED_CONTEXT((#12784,#12786,#12787))
REPRESENTATION_CONTEXT('','3D')
);
#12784=(
LENGTH_UNIT()
NAMED_UNIT(*)
SI_UNIT(.CENTI.,.METRE.)
);
#12786=(
NAMED_UNIT(*)
PLANE_ANGLE_UNIT()
SI_UNIT($,.RADIAN.)
);
#12787=(
NAMED_UNIT(*)
SI_UNIT($,.STERADIAN.)
SOLID_ANGLE_UNIT()
);
#12804=SHAPE_DEFINITION_REPRESENTATION(#12852,#12947);
#12852=PRODUCT_DEFINITION_SHAPE('',$,#12991);
#12947=SHAPE_REPRESENTATION('',(#7327),#12756);
#12974=PRODUCT_DEFINITION_CONTEXT('part definition',#13105,'design');
#12991=PRODUCT_DEFINITION('Cap Screw - M4x16','Cap Screw - M4x16',#13034,
#12974);
#13034=PRODUCT_DEFINITION_FORMATION('',$,#13123);
#13105=APPLICATION_CONTEXT(
'Core Data for Automotive Mechanical Design Process');
#13106=PRODUCT_CONTEXT('part definition',#13105,'mechanical');
#13123=PRODUCT('Cap Screw - M4x16','Cap Screw - M4x16',
'Cap Screw - M4x16',(#13106));
#13213=COLOUR_RGB('Black',0.12,0.14,0.17);
#13214=FILL_AREA_STYLE_COLOUR('',#13213);
#13215=FILL_AREA_STYLE('',(#13214));
#13216=SURFACE_STYLE_FILL_AREA(#13215);
#13217=SURFACE_SIDE_STYLE('',(#13216));
#13218=SURFACE_STYLE_USAGE(.BOTH.,#13217);
#13219=PRESENTATION_STYLE_ASSIGNMENT((#13218));
ENDSEC;
END-ISO-10303-21;
